ISO-10303-21;
HEADER;
/* Generated by software containing ST-Developer
 * from STEP Tools, Inc. (www.steptools.com) 
 */

FILE_DESCRIPTION(
/* description */ (''),
/* implementation_level */ '2;1');

FILE_NAME(
/* name */ '13_Shaft_Lip_Seal_30x47x7.step',
/* time_stamp */ '2026-10-26T07:49:00-07:00',
/* author */ (''),
/* organization */ (''),
/* preprocessor_version */ 'ST-DEVELOPER v20.2',
/* originating_system */ 'Autodesk Translation Framework v15.15.0.0',
/* authorisation */ '');

FILE_SCHEMA (('AUTOMOTIVE_DESIGN { 1 0 10303 214 3 1 1 }'));
ENDSEC;

DATA;
#10=MECHANICAL_DESIGN_GEOMETRIC_PRESENTATION_REPRESENTATION('',(#186),#38507);
#156=SHAPE_REPRESENTATION_RELATIONSHIP('SRR','None',#38584,#171);
#171=ADVANCED_BREP_SHAPE_REPRESENTATION('',(#201),#38501);
#186=STYLED_ITEM('',(#38727),#201);
#201=MANIFOLD_SOLID_BREP('Body1',#15080);
#503=FACE_BOUND('',#3134,.T.);
#504=FACE_BOUND('',#3138,.T.);
#505=FACE_BOUND('',#3142,.T.);
#506=FACE_BOUND('',#3145,.T.);
#798=PLANE('',#16234);
#799=PLANE('',#16242);
#800=PLANE('',#16248);
#801=PLANE('',#16251);
#1502=CYLINDRICAL_SURFACE('',#16236,20.5);
#1503=CYLINDRICAL_SURFACE('',#16246,15.);
#1504=CYLINDRICAL_SURFACE('',#16250,23.52);
#2159=FACE_OUTER_BOUND('',#3132,.T.);
#2160=FACE_OUTER_BOUND('',#3133,.T.);
#2161=FACE_OUTER_BOUND('',#3135,.T.);
#2162=FACE_OUTER_BOUND('',#3136,.T.);
#2163=FACE_OUTER_BOUND('',#3137,.T.);
#2164=FACE_OUTER_BOUND('',#3139,.T.);
#2165=FACE_OUTER_BOUND('',#3140,.T.);
#2166=FACE_OUTER_BOUND('',#3141,.T.);
#2167=FACE_OUTER_BOUND('',#3143,.T.);
#2168=FACE_OUTER_BOUND('',#3144,.T.);
#2169=FACE_OUTER_BOUND('',#3146,.T.);
#3132=EDGE_LOOP('',(#12445,#12446,#12447,#12448,#12449));
#3133=EDGE_LOOP('',(#12450));
#3134=EDGE_LOOP('',(#12451));
#3135=EDGE_LOOP('',(#12452,#12453,#12454,#12455,#12456));
#3136=EDGE_LOOP('',(#12457,#12458,#12459,#12460,#12461));
#3137=EDGE_LOOP('',(#12462));
#3138=EDGE_LOOP('',(#12463));
#3139=EDGE_LOOP('',(#12464,#12465,#12466,#12467,#12468));
#3140=EDGE_LOOP('',(#12469,#12470,#12471,#12472));
#3141=EDGE_LOOP('',(#12473));
#3142=EDGE_LOOP('',(#12474));
#3143=EDGE_LOOP('',(#12475,#12476,#12477,#12478));
#3144=EDGE_LOOP('',(#12479));
#3145=EDGE_LOOP('',(#12480));
#3146=EDGE_LOOP('',(#12481,#12482,#12483,#12484));
#4122=LINE('',#26954,#5191);
#4123=LINE('',#26961,#5192);
#4124=LINE('',#26969,#5193);
#4125=LINE('',#26977,#5194);
#4126=LINE('',#26981,#5195);
#4127=LINE('',#26986,#5196);
#4128=LINE('',#26991,#5197);
#5191=VECTOR('',#19327,20.64);
#5192=VECTOR('',#19336,20.5);
#5193=VECTOR('',#19345,16.9764870412073);
#5194=VECTOR('',#19356,17.75);
#5195=VECTOR('',#19361,15.);
#5196=VECTOR('',#19368,23.52);
#5197=VECTOR('',#19375,16.5);
#6101=CIRCLE('',#16231,20.5);
#6102=CIRCLE('',#16232,20.5);
#6103=CIRCLE('',#16233,20.78);
#6104=CIRCLE('',#16235,23.52);
#6105=CIRCLE('',#16237,20.5);
#6106=CIRCLE('',#16239,17.2329740824146);
#6107=CIRCLE('',#16240,17.2329740824146);
#6108=CIRCLE('',#16241,16.72);
#6109=CIRCLE('',#16243,15.);
#6110=CIRCLE('',#16245,18.5);
#6111=CIRCLE('',#16247,15.);
#6112=CIRCLE('',#16249,23.52);
#6113=CIRCLE('',#16252,18.);
#7106=VERTEX_POINT('',#26949);
#7107=VERTEX_POINT('',#26950);
#7108=VERTEX_POINT('',#26953);
#7109=VERTEX_POINT('',#26957);
#7110=VERTEX_POINT('',#26960);
#7111=VERTEX_POINT('',#26964);
#7112=VERTEX_POINT('',#26965);
#7113=VERTEX_POINT('',#26968);
#7114=VERTEX_POINT('',#26972);
#7115=VERTEX_POINT('',#26975);
#7116=VERTEX_POINT('',#26979);
#7117=VERTEX_POINT('',#26983);
#7118=VERTEX_POINT('',#26988);
#8971=EDGE_CURVE('',#7106,#7107,#6101,.T.);
#8972=EDGE_CURVE('',#7107,#7106,#6102,.T.);
#8973=EDGE_CURVE('',#7106,#7108,#4122,.T.);
#8974=EDGE_CURVE('',#7108,#7108,#6103,.T.);
#8975=EDGE_CURVE('',#7109,#7109,#6104,.T.);
#8976=EDGE_CURVE('',#7107,#7110,#4123,.T.);
#8977=EDGE_CURVE('',#7110,#7110,#6105,.T.);
#8978=EDGE_CURVE('',#7111,#7112,#6106,.T.);
#8979=EDGE_CURVE('',#7112,#7111,#6107,.T.);
#8980=EDGE_CURVE('',#7111,#7113,#4124,.T.);
#8981=EDGE_CURVE('',#7113,#7113,#6108,.T.);
#8982=EDGE_CURVE('',#7114,#7114,#6109,.T.);
#8983=EDGE_CURVE('',#7115,#7115,#6110,.T.);
#8984=EDGE_CURVE('',#7115,#7112,#4125,.T.);
#8985=EDGE_CURVE('',#7116,#7116,#6111,.T.);
#8986=EDGE_CURVE('',#7116,#7114,#4126,.T.);
#8987=EDGE_CURVE('',#7117,#7117,#6112,.T.);
#8988=EDGE_CURVE('',#7109,#7117,#4127,.T.);
#8989=EDGE_CURVE('',#7118,#7118,#6113,.T.);
#8990=EDGE_CURVE('',#7118,#7116,#4128,.T.);
#12445=ORIENTED_EDGE('',*,*,#8971,.T.);
#12446=ORIENTED_EDGE('',*,*,#8972,.T.);
#12447=ORIENTED_EDGE('',*,*,#8973,.T.);
#12448=ORIENTED_EDGE('',*,*,#8974,.T.);
#12449=ORIENTED_EDGE('',*,*,#8973,.F.);
#12450=ORIENTED_EDGE('',*,*,#8975,.T.);
#12451=ORIENTED_EDGE('',*,*,#8974,.F.);
#12452=ORIENTED_EDGE('',*,*,#8971,.F.);
#12453=ORIENTED_EDGE('',*,*,#8972,.F.);
#12454=ORIENTED_EDGE('',*,*,#8976,.T.);
#12455=ORIENTED_EDGE('',*,*,#8977,.F.);
#12456=ORIENTED_EDGE('',*,*,#8976,.F.);
#12457=ORIENTED_EDGE('',*,*,#8978,.T.);
#12458=ORIENTED_EDGE('',*,*,#8979,.T.);
#12459=ORIENTED_EDGE('',*,*,#8980,.T.);
#12460=ORIENTED_EDGE('',*,*,#8981,.T.);
#12461=ORIENTED_EDGE('',*,*,#8980,.F.);
#12462=ORIENTED_EDGE('',*,*,#8981,.F.);
#12463=ORIENTED_EDGE('',*,*,#8982,.T.);
#12464=ORIENTED_EDGE('',*,*,#8983,.F.);
#12465=ORIENTED_EDGE('',*,*,#8984,.T.);
#12466=ORIENTED_EDGE('',*,*,#8978,.F.);
#12467=ORIENTED_EDGE('',*,*,#8979,.F.);
#12468=ORIENTED_EDGE('',*,*,#8984,.F.);
#12469=ORIENTED_EDGE('',*,*,#8985,.T.);
#12470=ORIENTED_EDGE('',*,*,#8986,.T.);
#12471=ORIENTED_EDGE('',*,*,#8982,.F.);
#12472=ORIENTED_EDGE('',*,*,#8986,.F.);
#12473=ORIENTED_EDGE('',*,*,#8987,.F.);
#12474=ORIENTED_EDGE('',*,*,#8983,.T.);
#12475=ORIENTED_EDGE('',*,*,#8975,.F.);
#12476=ORIENTED_EDGE('',*,*,#8988,.T.);
#12477=ORIENTED_EDGE('',*,*,#8987,.T.);
#12478=ORIENTED_EDGE('',*,*,#8988,.F.);
#12479=ORIENTED_EDGE('',*,*,#8977,.T.);
#12480=ORIENTED_EDGE('',*,*,#8989,.F.);
#12481=ORIENTED_EDGE('',*,*,#8989,.T.);
#12482=ORIENTED_EDGE('',*,*,#8990,.T.);
#12483=ORIENTED_EDGE('',*,*,#8985,.F.);
#12484=ORIENTED_EDGE('',*,*,#8990,.F.);
#14171=CONICAL_SURFACE('',#16230,20.64,0.785398163397448);
#14172=CONICAL_SURFACE('',#16238,16.9764870412073,1.27679502502111);
#14173=CONICAL_SURFACE('',#16244,17.75,0.982793723247329);
#14174=CONICAL_SURFACE('',#16253,16.5,0.982793723247329);
#14726=ADVANCED_FACE('',(#2159),#14171,.F.);
#14727=ADVANCED_FACE('',(#2160,#503),#798,.T.);
#14728=ADVANCED_FACE('',(#2161),#1502,.F.);
#14729=ADVANCED_FACE('',(#2162),#14172,.T.);
#14730=ADVANCED_FACE('',(#2163,#504),#799,.T.);
#14731=ADVANCED_FACE('',(#2164),#14173,.T.);
#14732=ADVANCED_FACE('',(#2165),#1503,.F.);
#14733=ADVANCED_FACE('',(#2166,#505),#800,.T.);
#14734=ADVANCED_FACE('',(#2167),#1504,.T.);
#14735=ADVANCED_FACE('',(#2168,#506),#801,.T.);
#14736=ADVANCED_FACE('',(#2169),#14174,.F.);
#15080=CLOSED_SHELL('',(#14726,#14727,#14728,#14729,#14730,#14731,#14732,
#14733,#14734,#14735,#14736));
#16229=AXIS2_PLACEMENT_3D('',#26947,#19319,#19320);
#16230=AXIS2_PLACEMENT_3D('',#26948,#19321,#19322);
#16231=AXIS2_PLACEMENT_3D('',#26951,#19323,#19324);
#16232=AXIS2_PLACEMENT_3D('',#26952,#19325,#19326);
#16233=AXIS2_PLACEMENT_3D('',#26955,#19328,#19329);
#16234=AXIS2_PLACEMENT_3D('',#26956,#19330,#19331);
#16235=AXIS2_PLACEMENT_3D('',#26958,#19332,#19333);
#16236=AXIS2_PLACEMENT_3D('',#26959,#19334,#19335);
#16237=AXIS2_PLACEMENT_3D('',#26962,#19337,#19338);
#16238=AXIS2_PLACEMENT_3D('',#26963,#19339,#19340);
#16239=AXIS2_PLACEMENT_3D('',#26966,#19341,#19342);
#16240=AXIS2_PLACEMENT_3D('',#26967,#19343,#19344);
#16241=AXIS2_PLACEMENT_3D('',#26970,#19346,#19347);
#16242=AXIS2_PLACEMENT_3D('',#26971,#19348,#19349);
#16243=AXIS2_PLACEMENT_3D('',#26973,#19350,#19351);
#16244=AXIS2_PLACEMENT_3D('',#26974,#19352,#19353);
#16245=AXIS2_PLACEMENT_3D('',#26976,#19354,#19355);
#16246=AXIS2_PLACEMENT_3D('',#26978,#19357,#19358);
#16247=AXIS2_PLACEMENT_3D('',#26980,#19359,#19360);
#16248=AXIS2_PLACEMENT_3D('',#26982,#19362,#19363);
#16249=AXIS2_PLACEMENT_3D('',#26984,#19364,#19365);
#16250=AXIS2_PLACEMENT_3D('',#26985,#19366,#19367);
#16251=AXIS2_PLACEMENT_3D('',#26987,#19369,#19370);
#16252=AXIS2_PLACEMENT_3D('',#26989,#19371,#19372);
#16253=AXIS2_PLACEMENT_3D('',#26990,#19373,#19374);
#19319=DIRECTION('axis',(0.,0.,1.));
#19320=DIRECTION('refdir',(1.,0.,0.));
#19321=DIRECTION('center_axis',(1.,0.,0.));
#19322=DIRECTION('ref_axis',(0.,-1.,0.));
#19323=DIRECTION('center_axis',(-1.,0.,0.));
#19324=DIRECTION('ref_axis',(0.,-1.,0.));
#19325=DIRECTION('center_axis',(-1.,0.,0.));
#19326=DIRECTION('ref_axis',(0.,-1.,0.));
#19327=DIRECTION('',(0.707106781186547,0.707106781186547,-8.65956056235493E-17));
#19328=DIRECTION('center_axis',(1.,0.,0.));
#19329=DIRECTION('ref_axis',(0.,-1.,0.));
#19330=DIRECTION('center_axis',(1.,0.,0.));
#19331=DIRECTION('ref_axis',(0.,0.,-1.));
#19332=DIRECTION('center_axis',(1.,0.,0.));
#19333=DIRECTION('ref_axis',(0.,0.,-1.));
#19334=DIRECTION('center_axis',(1.,0.,0.));
#19335=DIRECTION('ref_axis',(0.,1.,0.));
#19336=DIRECTION('',(-1.,0.,0.));
#19337=DIRECTION('center_axis',(1.,0.,0.));
#19338=DIRECTION('ref_axis',(0.,0.,-1.));
#19339=DIRECTION('center_axis',(1.,0.,-6.79398744629287E-15));
#19340=DIRECTION('ref_axis',(0.,-1.,-3.10787303913223E-17));
#19341=DIRECTION('center_axis',(-1.,0.,0.));
#19342=DIRECTION('ref_axis',(0.,-1.,-6.12323399573677E-17));
#19343=DIRECTION('center_axis',(-1.,0.,0.));
#19344=DIRECTION('ref_axis',(0.,-1.,-6.12323399573677E-17));
#19345=DIRECTION('',(-0.289784148688431,-0.957092026489052,1.8218346946E-15));
#19346=DIRECTION('center_axis',(1.,0.,0.));
#19347=DIRECTION('ref_axis',(0.,-1.,0.));
#19348=DIRECTION('center_axis',(-1.,0.,0.));
#19349=DIRECTION('ref_axis',(0.,0.,1.));
#19350=DIRECTION('center_axis',(1.,0.,0.));
#19351=DIRECTION('ref_axis',(0.,0.,-1.));
#19352=DIRECTION('center_axis',(1.,0.,0.));
#19353=DIRECTION('ref_axis',(0.,1.,0.));
#19354=DIRECTION('center_axis',(1.,0.,0.));
#19355=DIRECTION('ref_axis',(0.,0.,-1.));
#19356=DIRECTION('',(-0.554700196225229,0.832050294337844,1.01896772969045E-16));
#19357=DIRECTION('center_axis',(1.,0.,0.));
#19358=DIRECTION('ref_axis',(0.,1.,0.));
#19359=DIRECTION('center_axis',(1.,0.,0.));
#19360=DIRECTION('ref_axis',(0.,0.,-1.));
#19361=DIRECTION('',(-1.,0.,0.));
#19362=DIRECTION('center_axis',(-1.,0.,0.));
#19363=DIRECTION('ref_axis',(0.,0.,1.));
#19364=DIRECTION('center_axis',(1.,0.,0.));
#19365=DIRECTION('ref_axis',(0.,0.,-1.));
#19366=DIRECTION('center_axis',(1.,0.,0.));
#19367=DIRECTION('ref_axis',(0.,1.,0.));
#19368=DIRECTION('',(-1.,0.,0.));
#19369=DIRECTION('center_axis',(1.,0.,0.));
#19370=DIRECTION('ref_axis',(0.,0.,-1.));
#19371=DIRECTION('center_axis',(1.,0.,0.));
#19372=DIRECTION('ref_axis',(0.,0.,-1.));
#19373=DIRECTION('center_axis',(1.,0.,0.));
#19374=DIRECTION('ref_axis',(0.,1.,0.));
#19375=DIRECTION('',(-0.554700196225229,0.832050294337844,1.01896772969045E-16));
#26947=CARTESIAN_POINT('',(0.,0.,0.));
#26948=CARTESIAN_POINT('Origin',(6.86,0.,0.));
#26949=CARTESIAN_POINT('',(6.72,20.5,-2.51052593825207E-15));
#26950=CARTESIAN_POINT('',(6.72,-20.5,-2.51052593825207E-15));
#26951=CARTESIAN_POINT('Origin',(6.72,0.,0.));
#26952=CARTESIAN_POINT('Origin',(6.72,0.,0.));
#26953=CARTESIAN_POINT('',(7.,20.78,2.5448160486282E-15));
#26954=CARTESIAN_POINT('',(6.86,20.64,-2.52767099344014E-15));
#26955=CARTESIAN_POINT('Origin',(7.,0.,0.));
#26956=CARTESIAN_POINT('Origin',(7.,20.5,0.));
#26957=CARTESIAN_POINT('',(7.,-23.52,-2.88036927159457E-15));
#26958=CARTESIAN_POINT('Origin',(7.,0.,0.));
#26959=CARTESIAN_POINT('Origin',(6.25,0.,0.));
#26960=CARTESIAN_POINT('',(5.5,-20.5,-2.51052593825207E-15));
#26961=CARTESIAN_POINT('',(6.25,-20.5,-2.51052593825207E-15));
#26962=CARTESIAN_POINT('Origin',(5.5,0.,0.));
#26963=CARTESIAN_POINT('Origin',(0.0776580274715325,0.,-5.27607663745458E-16));
#26964=CARTESIAN_POINT('',(0.155316054943065,17.2329740824146,-2.11043065498183E-15));
#26965=CARTESIAN_POINT('',(0.155316054943064,-17.2329740824146,-2.11043065498183E-15));
#26966=CARTESIAN_POINT('Origin',(0.155316054943065,0.,-1.05521532749092E-15));
#26967=CARTESIAN_POINT('Origin',(0.155316054943065,0.,-1.05521532749092E-15));
#26968=CARTESIAN_POINT('',(0.,16.72,2.04760944817437E-15));
#26969=CARTESIAN_POINT('',(0.0776580274715325,16.9764870412073,2.0790200515781E-15));
#26970=CARTESIAN_POINT('Origin',(0.,0.,0.));
#26971=CARTESIAN_POINT('Origin',(0.,17.,0.));
#26972=CARTESIAN_POINT('',(0.,-15.,-1.83697019872103E-15));
#26973=CARTESIAN_POINT('Origin',(0.,0.,0.));
#26974=CARTESIAN_POINT('Origin',(0.5,0.,0.));
#26975=CARTESIAN_POINT('',(1.,-18.5,-2.2655965784226E-15));
#26976=CARTESIAN_POINT('Origin',(1.,0.,0.));
#26977=CARTESIAN_POINT('',(0.5,-17.75,-2.17374806848655E-15));
#26978=CARTESIAN_POINT('Origin',(1.75,0.,0.));
#26979=CARTESIAN_POINT('',(3.5,-15.,-1.83697019872103E-15));
#26980=CARTESIAN_POINT('Origin',(3.5,0.,0.));
#26981=CARTESIAN_POINT('',(1.75,-15.,-1.83697019872103E-15));
#26982=CARTESIAN_POINT('Origin',(1.,23.52,0.));
#26983=CARTESIAN_POINT('',(1.,-23.52,-2.88036927159457E-15));
#26984=CARTESIAN_POINT('Origin',(1.,0.,0.));
#26985=CARTESIAN_POINT('Origin',(4.,0.,0.));
#26986=CARTESIAN_POINT('',(4.,-23.52,-2.88036927159457E-15));
#26987=CARTESIAN_POINT('Origin',(5.5,18.,0.));
#26988=CARTESIAN_POINT('',(5.5,-18.,-2.20436423846524E-15));
#26989=CARTESIAN_POINT('Origin',(5.5,0.,0.));
#26990=CARTESIAN_POINT('Origin',(4.5,0.,0.));
#26991=CARTESIAN_POINT('',(4.5,-16.5,-2.02066721859313E-15));
#38484=UNCERTAINTY_MEASURE_WITH_UNIT(LENGTH_MEASURE(0.01),#38508,
'DISTANCE_ACCURACY_VALUE',
'Maximum model space distance between geometric entities at asserted c
onnectivities');
#38490=UNCERTAINTY_MEASURE_WITH_UNIT(LENGTH_MEASURE(0.01),#38508,
'DISTANCE_ACCURACY_VALUE',
'Maximum model space distance between geometric entities at asserted c
onnectivities');
#38501=(
GEOMETRIC_REPRESENTATION_CONTEXT(3)
GLOBAL_UNCERTAINTY_ASSIGNED_CONTEXT((#38484))
GLOBAL_UNIT_ASSIGNED_CONTEXT((#38508,#38510,#38511))
REPRESENTATION_CONTEXT('','3D')
);
#38507=(
GEOMETRIC_REPRESENTATION_CONTEXT(3)
GLOBAL_UNCERTAINTY_ASSIGNED_CONTEXT((#38490))
GLOBAL_UNIT_ASSIGNED_CONTEXT((#38508,#38510,#38511))
REPRESENTATION_CONTEXT('','3D')
);
#38508=(
LENGTH_UNIT()
NAMED_UNIT(*)
SI_UNIT(.MILLI.,.METRE.)
);
#38510=(
NAMED_UNIT(*)
PLANE_ANGLE_UNIT()
SI_UNIT($,.RADIAN.)
);
#38511=(
NAMED_UNIT(*)
SI_UNIT($,.STERADIAN.)
SOLID_ANGLE_UNIT()
);
#38522=SHAPE_DEFINITION_REPRESENTATION(#38538,#38584);
#38538=PRODUCT_DEFINITION_SHAPE('',$,#38601);
#38584=SHAPE_REPRESENTATION('',(#16229),#38501);
#38590=PRODUCT_DEFINITION_CONTEXT('part definition',#38640,'design');
#38601=PRODUCT_DEFINITION('2026-10-26-01-10-56-411',
'13_Shaft_Lip_Seal_30x47x7',#38617,#38590);
#38617=PRODUCT_DEFINITION_FORMATION('',$,#38652);
#38640=APPLICATION_CONTEXT(
'Core Data for Automotive Mechanical Design Process');
#38641=PRODUCT_CONTEXT('part definition',#38640,'mechanical');
#38652=PRODUCT('2026-10-26-01-10-56-411','13_Shaft_Lip_Seal_30x47x7',$,
(#38641));
#38721=COLOUR_RGB('Black',0.12,0.14,0.17);
#38722=FILL_AREA_STYLE_COLOUR('',#38721);
#38723=FILL_AREA_STYLE('',(#38722));
#38724=SURFACE_STYLE_FILL_AREA(#38723);
#38725=SURFACE_SIDE_STYLE('',(#38724));
#38726=SURFACE_STYLE_USAGE(.BOTH.,#38725);
#38727=PRESENTATION_STYLE_ASSIGNMENT((#38726));
ENDSEC;
END-ISO-10303-21;
